ISO-10303-21;
HEADER;
/* Generated by software containing ST-Developer
 * from STEP Tools, Inc. (www.steptools.com) 
 */

FILE_DESCRIPTION(
/* description */ (''),
/* implementation_level */ '2;1');

FILE_NAME(
/* name */ 'GLAND_NUT.step',
/* time_stamp */ '2026-10-04T02:10:06-07:00',
/* author */ (''),
/* organization */ (''),
/* preprocessor_version */ 'ST-DEVELOPER v20.2',
/* originating_system */ 'Autodesk Translation Framework v15.15.0.0',
/* authorisation */ '');

FILE_SCHEMA (('AUTOMOTIVE_DESIGN { 1 0 10303 214 3 1 1 }'));
ENDSEC;

DATA;
#10=MECHANICAL_DESIGN_GEOMETRIC_PRESENTATION_REPRESENTATION('',(#148),#9668);
#126=SHAPE_REPRESENTATION_RELATIONSHIP('SRR','None',#9719,#137);
#137=ADVANCED_BREP_SHAPE_REPRESENTATION('',(#159),#9664);
#148=STYLED_ITEM('',(#9775),#159);
#159=MANIFOLD_SOLID_BREP('Body1',#3888);
#176=CONICAL_SURFACE('',#4320,34.6410161513776,0.255722691902349);
#256=FACE_BOUND('',#1227,.T.);
#257=FACE_BOUND('',#1230,.T.);
#258=FACE_BOUND('',#1238,.T.);
#259=FACE_BOUND('',#1242,.T.);
#322=PLANE('',#4293);
#323=PLANE('',#4294);
#324=PLANE('',#4295);
#325=PLANE('',#4296);
#326=PLANE('',#4297);
#327=PLANE('',#4298);
#328=PLANE('',#4299);
#329=PLANE('',#4303);
#330=PLANE('',#4317);
#331=PLANE('',#4323);
#488=LINE('',#6873,#679);
#489=LINE('',#6921,#680);
#490=LINE('',#6922,#681);
#491=LINE('',#6926,#682);
#492=LINE('',#6964,#683);
#493=LINE('',#7005,#684);
#494=LINE('',#7006,#685);
#495=LINE('',#7010,#686);
#496=LINE('',#7048,#687);
#497=LINE('',#7052,#688);
#498=LINE('',#7090,#689);
#499=LINE('',#7129,#690);
#500=LINE('',#7136,#691);
#501=LINE('',#7158,#692);
#502=LINE('',#7162,#693);
#503=LINE('',#7167,#694);
#679=VECTOR('',#5146,34.6410161513776);
#680=VECTOR('',#5147,34.6410161513776);
#681=VECTOR('',#5148,39.9999999999996);
#682=VECTOR('',#5151,34.6410161513776);
#683=VECTOR('',#5152,40.0000000000001);
#684=VECTOR('',#5155,40.0000000000001);
#685=VECTOR('',#5156,34.6410161513776);
#686=VECTOR('',#5159,34.6410161513776);
#687=VECTOR('',#5160,40.0000000000001);
#688=VECTOR('',#5163,34.6410161513776);
#689=VECTOR('',#5164,40.0000000000001);
#690=VECTOR('',#5167,40.0000000000001);
#691=VECTOR('',#5176,26.);
#692=VECTOR('',#5213,34.6410161513776);
#693=VECTOR('',#5218,12.);
#694=VECTOR('',#5225,10.);
#804=CYLINDRICAL_SURFACE('',#4301,26.);
#805=CYLINDRICAL_SURFACE('',#4321,12.);
#806=CYLINDRICAL_SURFACE('',#4325,10.);
#936=FACE_OUTER_BOUND('',#1220,.T.);
#937=FACE_OUTER_BOUND('',#1221,.T.);
#938=FACE_OUTER_BOUND('',#1222,.T.);
#939=FACE_OUTER_BOUND('',#1223,.T.);
#940=FACE_OUTER_BOUND('',#1224,.T.);
#941=FACE_OUTER_BOUND('',#1225,.T.);
#942=FACE_OUTER_BOUND('',#1226,.T.);
#943=FACE_OUTER_BOUND('',#1228,.T.);
#944=FACE_OUTER_BOUND('',#1229,.T.);
#945=FACE_OUTER_BOUND('',#1231,.T.);
#946=FACE_OUTER_BOUND('',#1232,.T.);
#947=FACE_OUTER_BOUND('',#1233,.T.);
#948=FACE_OUTER_BOUND('',#1234,.T.);
#949=FACE_OUTER_BOUND('',#1235,.T.);
#950=FACE_OUTER_BOUND('',#1236,.T.);
#951=FACE_OUTER_BOUND('',#1237,.T.);
#952=FACE_OUTER_BOUND('',#1239,.T.);
#953=FACE_OUTER_BOUND('',#1240,.T.);
#954=FACE_OUTER_BOUND('',#1241,.T.);
#955=FACE_OUTER_BOUND('',#1243,.T.);
#1220=EDGE_LOOP('',(#3139,#3140,#3141,#3142,#3143));
#1221=EDGE_LOOP('',(#3144,#3145,#3146,#3147,#3148));
#1222=EDGE_LOOP('',(#3149,#3150,#3151,#3152,#3153));
#1223=EDGE_LOOP('',(#3154,#3155,#3156,#3157,#3158));
#1224=EDGE_LOOP('',(#3159,#3160,#3161,#3162,#3163));
#1225=EDGE_LOOP('',(#3164,#3165,#3166,#3167,#3168));
#1226=EDGE_LOOP('',(#3169,#3170,#3171,#3172,#3173,#3174));
#1227=EDGE_LOOP('',(#3175));
#1228=EDGE_LOOP('',(#3176,#3177,#3178,#3179));
#1229=EDGE_LOOP('',(#3180));
#1230=EDGE_LOOP('',(#3181));
#1231=EDGE_LOOP('',(#3182,#3183,#3184));
#1232=EDGE_LOOP('',(#3185,#3186,#3187));
#1233=EDGE_LOOP('',(#3188,#3189,#3190));
#1234=EDGE_LOOP('',(#3191,#3192,#3193));
#1235=EDGE_LOOP('',(#3194,#3195,#3196));
#1236=EDGE_LOOP('',(#3197,#3198,#3199));
#1237=EDGE_LOOP('',(#3200));
#1238=EDGE_LOOP('',(#3201));
#1239=EDGE_LOOP('',(#3202,#3203,#3204,#3205,#3206,#3207,#3208,#3209,#3210));
#1240=EDGE_LOOP('',(#3211,#3212,#3213,#3214));
#1241=EDGE_LOOP('',(#3215));
#1242=EDGE_LOOP('',(#3216));
#1243=EDGE_LOOP('',(#3217,#3218,#3219,#3220));
#1359=B_SPLINE_CURVE_WITH_KNOTS('',3,(#6875,#6876,#6877,#6878,#6879,#6880,
#6881,#6882,#6883,#6884,#6885,#6886,#6887,#6888,#6889,#6890,#6891,#6892,
#6893,#6894,#6895,#6896),.UNSPECIFIED.,.F.,.F.,(4,2,2,2,2,2,2,2,2,2,4),
(-2.09523377758369,-2.02727170738156,-1.95930963717942,-1.86537787624874,
-1.77144611531805,-1.61404940438782,-1.45665269345759,-1.09248952009319,
-0.728326346728794,-0.364163173364397,0.),.UNSPECIFIED.);
#1360=B_SPLINE_CURVE_WITH_KNOTS('',3,(#6898,#6899,#6900,#6901,#6902,#6903,
#6904,#6905,#6906,#6907,#6908,#6909,#6910,#6911,#6912,#6913,#6914,#6915,
#6916,#6917,#6918,#6919),.UNSPECIFIED.,.F.,.F.,(4,2,2,2,2,2,2,2,2,2,4),
(-8.38093511033477,-8.01677193697037,-7.65260876360598,-7.28844559024158,
-6.92428241687718,-6.76688570594695,-6.60948899501672,-6.51555723408603,
-6.42162547315535,-6.35366340295321,-6.28570133275108),.UNSPECIFIED.);
#1361=B_SPLINE_CURVE_WITH_KNOTS('',3,(#6928,#6929,#6930,#6931,#6932,#6933,
#6934,#6935,#6936,#6937,#6938,#6939,#6940,#6941,#6942,#6943,#6944,#6945),
 .UNSPECIFIED.,.F.,.F.,(4,2,2,2,2,2,2,2,4),(-2.1101163324575,-2.02379922393296,
-1.92362324243839,-1.76357162567649,-1.6035200089146,-1.20264000668595,
-0.801760004457301,-0.40088000222865,0.),.UNSPECIFIED.);
#1362=B_SPLINE_CURVE_WITH_KNOTS('',3,(#6946,#6947,#6948,#6949,#6950,#6951,
#6952,#6953,#6954,#6955,#6956,#6957,#6958,#6959,#6960,#6961,#6962,#6963),
 .UNSPECIFIED.,.F.,.F.,(4,2,2,2,2,2,2,2,4),(-8.44046532983,-8.03958532760135,
-7.6387053253727,-7.23782532314405,-6.8369453209154,-6.67689370415351,-6.51684208739162,
-6.41666610589705,-6.3303489973725),.UNSPECIFIED.);
#1363=B_SPLINE_CURVE_WITH_KNOTS('',3,(#6968,#6969,#6970,#6971,#6972,#6973,
#6974,#6975,#6976,#6977,#6978,#6979,#6980,#6981,#6982,#6983,#6984,#6985),
 .UNSPECIFIED.,.F.,.F.,(4,2,2,2,2,2,2,2,4),(-2.1101163324575,-2.02379922393296,
-1.92362324243838,-1.76357162567649,-1.6035200089146,-1.20264000668595,
-0.8017600044573,-0.40088000222865,0.),.UNSPECIFIED.);
#1364=B_SPLINE_CURVE_WITH_KNOTS('',3,(#6986,#6987,#6988,#6989,#6990,#6991,
#6992,#6993,#6994,#6995,#6996,#6997,#6998,#6999,#7000,#7001,#7002,#7003),
 .UNSPECIFIED.,.F.,.F.,(4,2,2,2,2,2,2,2,4),(-8.44046532983,-8.03958532760135,
-7.6387053253727,-7.23782532314405,-6.8369453209154,-6.67689370415351,-6.51684208739162,
-6.41666610589704,-6.3303489973725),.UNSPECIFIED.);
#1365=B_SPLINE_CURVE_WITH_KNOTS('',3,(#7012,#7013,#7014,#7015,#7016,#7017,
#7018,#7019,#7020,#7021,#7022,#7023,#7024,#7025,#7026,#7027,#7028,#7029),
 .UNSPECIFIED.,.F.,.F.,(4,2,2,2,2,2,2,2,4),(-2.11011633245751,-2.02379922393296,
-1.92362324243839,-1.7635716256765,-1.60352000891461,-1.20264000668595,
-0.801760004457303,-0.400880002228651,0.),.UNSPECIFIED.);
#1366=B_SPLINE_CURVE_WITH_KNOTS('',3,(#7030,#7031,#7032,#7033,#7034,#7035,
#7036,#7037,#7038,#7039,#7040,#7041,#7042,#7043,#7044,#7045,#7046,#7047),
 .UNSPECIFIED.,.F.,.F.,(4,2,2,2,2,2,2,2,4),(-8.44046532983002,-8.03958532760137,
-7.63870532537272,-7.23782532314407,-6.83694532091541,-6.67689370415352,
-6.51684208739163,-6.41666610589706,-6.33034899737251),.UNSPECIFIED.);
#1367=B_SPLINE_CURVE_WITH_KNOTS('',3,(#7054,#7055,#7056,#7057,#7058,#7059,
#7060,#7061,#7062,#7063,#7064,#7065,#7066,#7067,#7068,#7069,#7070,#7071),
 .UNSPECIFIED.,.F.,.F.,(4,2,2,2,2,2,2,2,4),(-2.1101163324575,-2.02379922393296,
-1.92362324243838,-1.76357162567649,-1.6035200089146,-1.20264000668595,
-0.801760004457301,-0.40088000222865,0.),.UNSPECIFIED.);
#1368=B_SPLINE_CURVE_WITH_KNOTS('',3,(#7072,#7073,#7074,#7075,#7076,#7077,
#7078,#7079,#7080,#7081,#7082,#7083,#7084,#7085,#7086,#7087,#7088,#7089),
 .UNSPECIFIED.,.F.,.F.,(4,2,2,2,2,2,2,2,4),(-8.44046532983,-8.03958532760135,
-7.6387053253727,-7.23782532314405,-6.8369453209154,-6.67689370415351,-6.51684208739162,
-6.41666610589705,-6.3303489973725),.UNSPECIFIED.);
#1369=B_SPLINE_CURVE_WITH_KNOTS('',3,(#7093,#7094,#7095,#7096,#7097,#7098,
#7099,#7100,#7101,#7102,#7103,#7104,#7105,#7106,#7107,#7108,#7109,#7110),
 .UNSPECIFIED.,.F.,.F.,(4,2,2,2,2,2,2,2,4),(-2.1101163324575,-2.02379922393296,
-1.92362324243838,-1.76357162567649,-1.6035200089146,-1.20264000668595,
-0.8017600044573,-0.40088000222865,0.),.UNSPECIFIED.);
#1370=B_SPLINE_CURVE_WITH_KNOTS('',3,(#7111,#7112,#7113,#7114,#7115,#7116,
#7117,#7118,#7119,#7120,#7121,#7122,#7123,#7124,#7125,#7126,#7127,#7128),
 .UNSPECIFIED.,.F.,.F.,(4,2,2,2,2,2,2,2,4),(-8.44046532983,-8.03958532760135,
-7.6387053253727,-7.23782532314405,-6.8369453209154,-6.67689370415351,-6.51684208739162,
-6.41666610589704,-6.3303489973725),.UNSPECIFIED.);
#1571=CIRCLE('',#4300,26.);
#1572=CIRCLE('',#4302,26.);
#1573=CIRCLE('',#4304,12.);
#1574=CIRCLE('',#4306,34.6410161513776);
#1575=CIRCLE('',#4308,34.6410161513776);
#1576=CIRCLE('',#4310,34.6410161513776);
#1577=CIRCLE('',#4312,34.6410161513776);
#1578=CIRCLE('',#4314,34.6410161513776);
#1579=CIRCLE('',#4316,34.6410161513776);
#1580=CIRCLE('',#4318,20.);
#1581=CIRCLE('',#4319,10.);
#1582=CIRCLE('',#4322,12.);
#1583=CIRCLE('',#4324,10.);
#1837=VERTEX_POINT('',#6871);
#1838=VERTEX_POINT('',#6872);
#1839=VERTEX_POINT('',#6874);
#1840=VERTEX_POINT('',#6897);
#1841=VERTEX_POINT('',#6920);
#1842=VERTEX_POINT('',#6924);
#1843=VERTEX_POINT('',#6925);
#1844=VERTEX_POINT('',#6927);
#1845=VERTEX_POINT('',#6966);
#1846=VERTEX_POINT('',#6967);
#1847=VERTEX_POINT('',#7004);
#1848=VERTEX_POINT('',#7008);
#1849=VERTEX_POINT('',#7009);
#1850=VERTEX_POINT('',#7011);
#1851=VERTEX_POINT('',#7050);
#1852=VERTEX_POINT('',#7051);
#1853=VERTEX_POINT('',#7053);
#1854=VERTEX_POINT('',#7092);
#1855=VERTEX_POINT('',#7131);
#1856=VERTEX_POINT('',#7134);
#1857=VERTEX_POINT('',#7138);
#1858=VERTEX_POINT('',#7153);
#1859=VERTEX_POINT('',#7155);
#1860=VERTEX_POINT('',#7160);
#1861=VERTEX_POINT('',#7164);
#2293=EDGE_CURVE('',#1837,#1838,#488,.T.);
#2294=EDGE_CURVE('',#1837,#1839,#1359,.T.);
#2295=EDGE_CURVE('',#1839,#1840,#1360,.T.);
#2296=EDGE_CURVE('',#1840,#1841,#489,.T.);
#2297=EDGE_CURVE('',#1841,#1838,#490,.T.);
#2298=EDGE_CURVE('',#1842,#1843,#491,.T.);
#2299=EDGE_CURVE('',#1842,#1844,#1361,.T.);
#2300=EDGE_CURVE('',#1844,#1837,#1362,.T.);
#2301=EDGE_CURVE('',#1838,#1843,#492,.T.);
#2302=EDGE_CURVE('',#1845,#1846,#1363,.T.);
#2303=EDGE_CURVE('',#1846,#1842,#1364,.T.);
#2304=EDGE_CURVE('',#1843,#1847,#493,.T.);
#2305=EDGE_CURVE('',#1845,#1847,#494,.T.);
#2306=EDGE_CURVE('',#1848,#1849,#495,.T.);
#2307=EDGE_CURVE('',#1848,#1850,#1365,.T.);
#2308=EDGE_CURVE('',#1850,#1845,#1366,.T.);
#2309=EDGE_CURVE('',#1847,#1849,#496,.T.);
#2310=EDGE_CURVE('',#1851,#1852,#497,.T.);
#2311=EDGE_CURVE('',#1851,#1853,#1367,.T.);
#2312=EDGE_CURVE('',#1853,#1848,#1368,.T.);
#2313=EDGE_CURVE('',#1849,#1852,#498,.T.);
#2314=EDGE_CURVE('',#1840,#1854,#1369,.T.);
#2315=EDGE_CURVE('',#1854,#1851,#1370,.T.);
#2316=EDGE_CURVE('',#1852,#1841,#499,.T.);
#2317=EDGE_CURVE('',#1855,#1855,#1571,.T.);
#2318=EDGE_CURVE('',#1856,#1856,#1572,.T.);
#2319=EDGE_CURVE('',#1856,#1855,#500,.T.);
#2320=EDGE_CURVE('',#1857,#1857,#1573,.T.);
#2321=EDGE_CURVE('',#1839,#1854,#1574,.T.);
#2322=EDGE_CURVE('',#1844,#1839,#1575,.T.);
#2323=EDGE_CURVE('',#1846,#1844,#1576,.T.);
#2324=EDGE_CURVE('',#1850,#1846,#1577,.T.);
#2325=EDGE_CURVE('',#1853,#1850,#1578,.T.);
#2326=EDGE_CURVE('',#1854,#1853,#1579,.T.);
#2327=EDGE_CURVE('',#1858,#1858,#1580,.T.);
#2328=EDGE_CURVE('',#1859,#1859,#1581,.T.);
#2329=EDGE_CURVE('',#1854,#1858,#501,.T.);
#2330=EDGE_CURVE('',#1860,#1860,#1582,.T.);
#2331=EDGE_CURVE('',#1860,#1857,#502,.T.);
#2332=EDGE_CURVE('',#1861,#1861,#1583,.T.);
#2333=EDGE_CURVE('',#1861,#1859,#503,.T.);
#3139=ORIENTED_EDGE('',*,*,#2293,.F.);
#3140=ORIENTED_EDGE('',*,*,#2294,.T.);
#3141=ORIENTED_EDGE('',*,*,#2295,.T.);
#3142=ORIENTED_EDGE('',*,*,#2296,.T.);
#3143=ORIENTED_EDGE('',*,*,#2297,.T.);
#3144=ORIENTED_EDGE('',*,*,#2298,.F.);
#3145=ORIENTED_EDGE('',*,*,#2299,.T.);
#3146=ORIENTED_EDGE('',*,*,#2300,.T.);
#3147=ORIENTED_EDGE('',*,*,#2293,.T.);
#3148=ORIENTED_EDGE('',*,*,#2301,.T.);
#3149=ORIENTED_EDGE('',*,*,#2302,.T.);
#3150=ORIENTED_EDGE('',*,*,#2303,.T.);
#3151=ORIENTED_EDGE('',*,*,#2298,.T.);
#3152=ORIENTED_EDGE('',*,*,#2304,.T.);
#3153=ORIENTED_EDGE('',*,*,#2305,.F.);
#3154=ORIENTED_EDGE('',*,*,#2306,.F.);
#3155=ORIENTED_EDGE('',*,*,#2307,.T.);
#3156=ORIENTED_EDGE('',*,*,#2308,.T.);
#3157=ORIENTED_EDGE('',*,*,#2305,.T.);
#3158=ORIENTED_EDGE('',*,*,#2309,.T.);
#3159=ORIENTED_EDGE('',*,*,#2310,.F.);
#3160=ORIENTED_EDGE('',*,*,#2311,.T.);
#3161=ORIENTED_EDGE('',*,*,#2312,.T.);
#3162=ORIENTED_EDGE('',*,*,#2306,.T.);
#3163=ORIENTED_EDGE('',*,*,#2313,.T.);
#3164=ORIENTED_EDGE('',*,*,#2314,.T.);
#3165=ORIENTED_EDGE('',*,*,#2315,.T.);
#3166=ORIENTED_EDGE('',*,*,#2310,.T.);
#3167=ORIENTED_EDGE('',*,*,#2316,.T.);
#3168=ORIENTED_EDGE('',*,*,#2296,.F.);
#3169=ORIENTED_EDGE('',*,*,#2297,.F.);
#3170=ORIENTED_EDGE('',*,*,#2316,.F.);
#3171=ORIENTED_EDGE('',*,*,#2313,.F.);
#3172=ORIENTED_EDGE('',*,*,#2309,.F.);
#3173=ORIENTED_EDGE('',*,*,#2304,.F.);
#3174=ORIENTED_EDGE('',*,*,#2301,.F.);
#3175=ORIENTED_EDGE('',*,*,#2317,.F.);
#3176=ORIENTED_EDGE('',*,*,#2318,.F.);
#3177=ORIENTED_EDGE('',*,*,#2319,.T.);
#3178=ORIENTED_EDGE('',*,*,#2317,.T.);
#3179=ORIENTED_EDGE('',*,*,#2319,.F.);
#3180=ORIENTED_EDGE('',*,*,#2318,.T.);
#3181=ORIENTED_EDGE('',*,*,#2320,.F.);
#3182=ORIENTED_EDGE('',*,*,#2321,.T.);
#3183=ORIENTED_EDGE('',*,*,#2314,.F.);
#3184=ORIENTED_EDGE('',*,*,#2295,.F.);
#3185=ORIENTED_EDGE('',*,*,#2322,.T.);
#3186=ORIENTED_EDGE('',*,*,#2294,.F.);
#3187=ORIENTED_EDGE('',*,*,#2300,.F.);
#3188=ORIENTED_EDGE('',*,*,#2323,.T.);
#3189=ORIENTED_EDGE('',*,*,#2299,.F.);
#3190=ORIENTED_EDGE('',*,*,#2303,.F.);
#3191=ORIENTED_EDGE('',*,*,#2308,.F.);
#3192=ORIENTED_EDGE('',*,*,#2324,.T.);
#3193=ORIENTED_EDGE('',*,*,#2302,.F.);
#3194=ORIENTED_EDGE('',*,*,#2312,.F.);
#3195=ORIENTED_EDGE('',*,*,#2325,.T.);
#3196=ORIENTED_EDGE('',*,*,#2307,.F.);
#3197=ORIENTED_EDGE('',*,*,#2315,.F.);
#3198=ORIENTED_EDGE('',*,*,#2326,.T.);
#3199=ORIENTED_EDGE('',*,*,#2311,.F.);
#3200=ORIENTED_EDGE('',*,*,#2327,.F.);
#3201=ORIENTED_EDGE('',*,*,#2328,.F.);
#3202=ORIENTED_EDGE('',*,*,#2323,.F.);
#3203=ORIENTED_EDGE('',*,*,#2324,.F.);
#3204=ORIENTED_EDGE('',*,*,#2325,.F.);
#3205=ORIENTED_EDGE('',*,*,#2326,.F.);
#3206=ORIENTED_EDGE('',*,*,#2329,.T.);
#3207=ORIENTED_EDGE('',*,*,#2327,.T.);
#3208=ORIENTED_EDGE('',*,*,#2329,.F.);
#3209=ORIENTED_EDGE('',*,*,#2321,.F.);
#3210=ORIENTED_EDGE('',*,*,#2322,.F.);
#3211=ORIENTED_EDGE('',*,*,#2330,.F.);
#3212=ORIENTED_EDGE('',*,*,#2331,.T.);
#3213=ORIENTED_EDGE('',*,*,#2320,.T.);
#3214=ORIENTED_EDGE('',*,*,#2331,.F.);
#3215=ORIENTED_EDGE('',*,*,#2330,.T.);
#3216=ORIENTED_EDGE('',*,*,#2332,.F.);
#3217=ORIENTED_EDGE('',*,*,#2332,.T.);
#3218=ORIENTED_EDGE('',*,*,#2333,.T.);
#3219=ORIENTED_EDGE('',*,*,#2328,.T.);
#3220=ORIENTED_EDGE('',*,*,#2333,.F.);
#3643=TOROIDAL_SURFACE('',#4305,34.6410161513776,5.35898384862241);
#3644=TOROIDAL_SURFACE('',#4307,34.6410161513776,5.35898384862241);
#3645=TOROIDAL_SURFACE('',#4309,34.6410161513776,5.35898384862241);
#3646=TOROIDAL_SURFACE('',#4311,34.6410161513776,5.35898384862241);
#3647=TOROIDAL_SURFACE('',#4313,34.6410161513776,5.35898384862241);
#3648=TOROIDAL_SURFACE('',#4315,34.6410161513776,5.35898384862241);
#3784=ADVANCED_FACE('',(#936),#322,.F.);
#3785=ADVANCED_FACE('',(#937),#323,.F.);
#3786=ADVANCED_FACE('',(#938),#324,.F.);
#3787=ADVANCED_FACE('',(#939),#325,.F.);
#3788=ADVANCED_FACE('',(#940),#326,.F.);
#3789=ADVANCED_FACE('',(#941),#327,.F.);
#3790=ADVANCED_FACE('',(#942,#256),#328,.F.);
#3791=ADVANCED_FACE('',(#943),#804,.F.);
#3792=ADVANCED_FACE('',(#944,#257),#329,.T.);
#3793=ADVANCED_FACE('',(#945),#3643,.T.);
#3794=ADVANCED_FACE('',(#946),#3644,.T.);
#3795=ADVANCED_FACE('',(#947),#3645,.T.);
#3796=ADVANCED_FACE('',(#948),#3646,.T.);
#3797=ADVANCED_FACE('',(#949),#3647,.T.);
#3798=ADVANCED_FACE('',(#950),#3648,.T.);
#3799=ADVANCED_FACE('',(#951,#258),#330,.T.);
#3800=ADVANCED_FACE('',(#952),#176,.T.);
#3801=ADVANCED_FACE('',(#953),#805,.F.);
#3802=ADVANCED_FACE('',(#954,#259),#331,.T.);
#3803=ADVANCED_FACE('',(#955),#806,.F.);
#3888=CLOSED_SHELL('',(#3784,#3785,#3786,#3787,#3788,#3789,#3790,#3791,
#3792,#3793,#3794,#3795,#3796,#3797,#3798,#3799,#3800,#3801,#3802,#3803));
#4292=AXIS2_PLACEMENT_3D('',#6869,#5142,#5143);
#4293=AXIS2_PLACEMENT_3D('',#6870,#5144,#5145);
#4294=AXIS2_PLACEMENT_3D('',#6923,#5149,#5150);
#4295=AXIS2_PLACEMENT_3D('',#6965,#5153,#5154);
#4296=AXIS2_PLACEMENT_3D('',#7007,#5157,#5158);
#4297=AXIS2_PLACEMENT_3D('',#7049,#5161,#5162);
#4298=AXIS2_PLACEMENT_3D('',#7091,#5165,#5166);
#4299=AXIS2_PLACEMENT_3D('',#7130,#5168,#5169);
#4300=AXIS2_PLACEMENT_3D('',#7132,#5170,#5171);
#4301=AXIS2_PLACEMENT_3D('',#7133,#5172,#5173);
#4302=AXIS2_PLACEMENT_3D('',#7135,#5174,#5175);
#4303=AXIS2_PLACEMENT_3D('',#7137,#5177,#5178);
#4304=AXIS2_PLACEMENT_3D('',#7139,#5179,#5180);
#4305=AXIS2_PLACEMENT_3D('',#7140,#5181,#5182);
#4306=AXIS2_PLACEMENT_3D('',#7141,#5183,#5184);
#4307=AXIS2_PLACEMENT_3D('',#7142,#5185,#5186);
#4308=AXIS2_PLACEMENT_3D('',#7143,#5187,#5188);
#4309=AXIS2_PLACEMENT_3D('',#7144,#5189,#5190);
#4310=AXIS2_PLACEMENT_3D('',#7145,#5191,#5192);
#4311=AXIS2_PLACEMENT_3D('',#7146,#5193,#5194);
#4312=AXIS2_PLACEMENT_3D('',#7147,#5195,#5196);
#4313=AXIS2_PLACEMENT_3D('',#7148,#5197,#5198);
#4314=AXIS2_PLACEMENT_3D('',#7149,#5199,#5200);
#4315=AXIS2_PLACEMENT_3D('',#7150,#5201,#5202);
#4316=AXIS2_PLACEMENT_3D('',#7151,#5203,#5204);
#4317=AXIS2_PLACEMENT_3D('',#7152,#5205,#5206);
#4318=AXIS2_PLACEMENT_3D('',#7154,#5207,#5208);
#4319=AXIS2_PLACEMENT_3D('',#7156,#5209,#5210);
#4320=AXIS2_PLACEMENT_3D('',#7157,#5211,#5212);
#4321=AXIS2_PLACEMENT_3D('',#7159,#5214,#5215);
#4322=AXIS2_PLACEMENT_3D('',#7161,#5216,#5217);
#4323=AXIS2_PLACEMENT_3D('',#7163,#5219,#5220);
#4324=AXIS2_PLACEMENT_3D('',#7165,#5221,#5222);
#4325=AXIS2_PLACEMENT_3D('',#7166,#5223,#5224);
#5142=DIRECTION('axis',(0.,0.,1.));
#5143=DIRECTION('refdir',(1.,0.,0.));
#5144=DIRECTION('center_axis',(-0.866025403784441,0.,-0.499999999999995));
#5145=DIRECTION('ref_axis',(-0.499999999999995,0.,0.866025403784442));
#5146=DIRECTION('',(0.,-1.,0.));
#5147=DIRECTION('',(0.,-1.,0.));
#5148=DIRECTION('',(0.499999999999995,0.,-0.866025403784441));
#5149=DIRECTION('center_axis',(-0.866025403784438,0.,0.500000000000001));
#5150=DIRECTION('ref_axis',(0.500000000000001,0.,0.866025403784438));
#5151=DIRECTION('',(0.,-1.,0.));
#5152=DIRECTION('',(-0.500000000000001,0.,-0.866025403784438));
#5153=DIRECTION('center_axis',(3.29597460435593E-15,0.,1.));
#5154=DIRECTION('ref_axis',(1.,0.,-3.29597460435593E-15));
#5155=DIRECTION('',(-1.,0.,3.33066907387546E-15));
#5156=DIRECTION('',(0.,-1.,0.));
#5157=DIRECTION('center_axis',(0.866025403784442,0.,0.499999999999995));
#5158=DIRECTION('ref_axis',(0.499999999999995,0.,-0.866025403784442));
#5159=DIRECTION('',(0.,-1.,0.));
#5160=DIRECTION('',(-0.499999999999995,0.,0.866025403784441));
#5161=DIRECTION('center_axis',(0.866025403784435,0.,-0.500000000000007));
#5162=DIRECTION('ref_axis',(-0.500000000000007,0.,-0.866025403784435));
#5163=DIRECTION('',(0.,-1.,0.));
#5164=DIRECTION('',(0.500000000000007,0.,0.866025403784434));
#5165=DIRECTION('center_axis',(-1.04083408558608E-14,0.,-1.));
#5166=DIRECTION('ref_axis',(-1.,0.,1.04083408558608E-14));
#5167=DIRECTION('',(1.,0.,-1.04360964314765E-14));
#5168=DIRECTION('center_axis',(0.,1.,0.));
#5169=DIRECTION('ref_axis',(0.,0.,1.));
#5170=DIRECTION('center_axis',(0.,-1.,0.));
#5171=DIRECTION('ref_axis',(0.,0.,-1.));
#5172=DIRECTION('center_axis',(0.,-1.,0.));
#5173=DIRECTION('ref_axis',(0.,0.,-1.));
#5174=DIRECTION('center_axis',(0.,-1.,0.));
#5175=DIRECTION('ref_axis',(0.,0.,-1.));
#5176=DIRECTION('',(0.,-1.,0.));
#5177=DIRECTION('center_axis',(0.,-1.,0.));
#5178=DIRECTION('ref_axis',(0.,0.,-1.));
#5179=DIRECTION('center_axis',(0.,-1.,0.));
#5180=DIRECTION('ref_axis',(0.,0.,-1.));
#5181=DIRECTION('center_axis',(0.,-1.,0.));
#5182=DIRECTION('ref_axis',(0.,0.,-1.));
#5183=DIRECTION('center_axis',(0.,-1.,0.));
#5184=DIRECTION('ref_axis',(0.,0.,-1.));
#5185=DIRECTION('center_axis',(0.,-1.,0.));
#5186=DIRECTION('ref_axis',(0.,0.,-1.));
#5187=DIRECTION('center_axis',(0.,-1.,0.));
#5188=DIRECTION('ref_axis',(0.,0.,-1.));
#5189=DIRECTION('center_axis',(0.,-1.,0.));
#5190=DIRECTION('ref_axis',(0.,0.,-1.));
#5191=DIRECTION('center_axis',(0.,-1.,0.));
#5192=DIRECTION('ref_axis',(0.,0.,-1.));
#5193=DIRECTION('center_axis',(0.,-1.,0.));
#5194=DIRECTION('ref_axis',(0.,0.,-1.));
#5195=DIRECTION('center_axis',(0.,-1.,0.));
#5196=DIRECTION('ref_axis',(0.,0.,-1.));
#5197=DIRECTION('center_axis',(0.,-1.,0.));
#5198=DIRECTION('ref_axis',(0.,0.,-1.));
#5199=DIRECTION('center_axis',(0.,-1.,0.));
#5200=DIRECTION('ref_axis',(0.,0.,-1.));
#5201=DIRECTION('center_axis',(0.,-1.,0.));
#5202=DIRECTION('ref_axis',(0.,0.,-1.));
#5203=DIRECTION('center_axis',(0.,-1.,0.));
#5204=DIRECTION('ref_axis',(0.,0.,-1.));
#5205=DIRECTION('center_axis',(0.,1.,0.));
#5206=DIRECTION('ref_axis',(0.,0.,1.));
#5207=DIRECTION('center_axis',(0.,-1.,0.));
#5208=DIRECTION('ref_axis',(0.,0.,-1.));
#5209=DIRECTION('center_axis',(0.,1.,0.));
#5210=DIRECTION('ref_axis',(0.,0.,1.));
#5211=DIRECTION('center_axis',(0.,-1.,0.));
#5212=DIRECTION('ref_axis',(0.,0.,-1.));
#5213=DIRECTION('',(3.09767874512465E-17,0.967480747292902,-0.252944665129683));
#5214=DIRECTION('center_axis',(0.,-1.,0.));
#5215=DIRECTION('ref_axis',(0.,0.,-1.));
#5216=DIRECTION('center_axis',(0.,-1.,0.));
#5217=DIRECTION('ref_axis',(0.,0.,-1.));
#5218=DIRECTION('',(0.,-1.,0.));
#5219=DIRECTION('center_axis',(0.,-1.,0.));
#5220=DIRECTION('ref_axis',(0.,0.,-1.));
#5221=DIRECTION('center_axis',(0.,-1.,0.));
#5222=DIRECTION('ref_axis',(0.,0.,-1.));
#5223=DIRECTION('center_axis',(0.,1.,0.));
#5224=DIRECTION('ref_axis',(0.,0.,1.));
#5225=DIRECTION('',(0.,1.,0.));
#6869=CARTESIAN_POINT('',(0.,0.,0.));
#6870=CARTESIAN_POINT('Origin',(20.0000000000004,40.,34.6410161513773));
#6871=CARTESIAN_POINT('',(40.,34.6410161513776,-1.04083408558608E-14));
#6872=CARTESIAN_POINT('',(40.,0.,0.));
#6873=CARTESIAN_POINT('',(40.,34.6410161513776,0.));
#6874=CARTESIAN_POINT('',(30.0000000000001,40.,17.3205080756886));
#6875=CARTESIAN_POINT('Ctrl Pts',(40.,34.6410161513776,-8.88178419700125E-15));
#6876=CARTESIAN_POINT('Ctrl Pts',(40.,34.8675563853847,-8.94780562024841E-15));
#6877=CARTESIAN_POINT('Ctrl Pts',(39.9845496882855,35.1132553852053,0.0267607248823537));
#6878=CARTESIAN_POINT('Ctrl Pts',(39.9209089392646,35.5879596782423,0.136989735618295));
#6879=CARTESIAN_POINT('Ctrl Pts',(39.8729336465118,35.8170802394984,0.22008538017415));
#6880=CARTESIAN_POINT('Ctrl Pts',(39.7450039767544,36.292215920861,0.44166606798931));
#6881=CARTESIAN_POINT('Ctrl Pts',(39.6445377014013,36.5686663529566,0.615678761348116));
#6882=CARTESIAN_POINT('Ctrl Pts',(39.413570269859,37.0692605098588,1.01572608767312));
#6883=CARTESIAN_POINT('Ctrl Pts',(39.2834488566673,37.2941045349873,1.24110298647387));
#6884=CARTESIAN_POINT('Ctrl Pts',(38.9479833579045,37.7957977176563,1.82214627451743));
#6885=CARTESIAN_POINT('Ctrl Pts',(38.6995716833136,38.0825278600404,2.25240791610222));
#6886=CARTESIAN_POINT('Ctrl Pts',(38.1796891744627,38.5640991767506,3.15287083539827));
#6887=CARTESIAN_POINT('Ctrl Pts',(37.9085074292358,38.7601877193308,3.62257139621652));
#6888=CARTESIAN_POINT('Ctrl Pts',(37.077311811023,39.2690611683488,5.06224443798978));
#6889=CARTESIAN_POINT('Ctrl Pts',(36.4597275654282,39.4955705648851,6.13193172931402));
#6890=CARTESIAN_POINT('Ctrl Pts',(35.1851649957381,39.8044631544014,8.33953885744289));
#6891=CARTESIAN_POINT('Ctrl Pts',(34.5280891925476,39.885235330521,9.47762753299292));
#6892=CARTESIAN_POINT('Ctrl Pts',(33.2073007717862,39.9780696179776,11.7653001838004));
#6893=CARTESIAN_POINT('Ctrl Pts',(32.5438367467531,39.9905745886849,12.9144535841519));
#6894=CARTESIAN_POINT('Ctrl Pts',(31.2436555254328,40.001470043377,15.1664335185256));
#6895=CARTESIAN_POINT('Ctrl Pts',(30.6069386222742,40.,16.2692595448342));
#6896=CARTESIAN_POINT('Ctrl Pts',(30.0000000000002,40.,17.3205080756887));
#6897=CARTESIAN_POINT('',(20.0000000000004,34.6410161513776,34.6410161513773));
#6898=CARTESIAN_POINT('Ctrl Pts',(30.0000000000002,40.,17.3205080756887));
#6899=CARTESIAN_POINT('Ctrl Pts',(29.3930613777262,40.,18.3717566065431));
#6900=CARTESIAN_POINT('Ctrl Pts',(28.7563444745676,40.001470043377,19.4745826328517));
#6901=CARTESIAN_POINT('Ctrl Pts',(27.4561632532473,39.990574588685,21.7265625672254));
#6902=CARTESIAN_POINT('Ctrl Pts',(26.7926992282142,39.9780696179776,22.8757159675769));
#6903=CARTESIAN_POINT('Ctrl Pts',(25.4719108074528,39.885235330521,25.1633886183844));
#6904=CARTESIAN_POINT('Ctrl Pts',(24.8148350042623,39.8044631544014,26.3014772939344));
#6905=CARTESIAN_POINT('Ctrl Pts',(23.5402724345722,39.4955705648851,28.5090844220633));
#6906=CARTESIAN_POINT('Ctrl Pts',(22.9226881889774,39.2690611683488,29.5787717133875));
#6907=CARTESIAN_POINT('Ctrl Pts',(22.0914925707646,38.7601877193308,31.0184447551608));
#6908=CARTESIAN_POINT('Ctrl Pts',(21.8203108255377,38.5640991767506,31.4881453159791));
#6909=CARTESIAN_POINT('Ctrl Pts',(21.3004283166868,38.0825278600404,32.3886082352751));
#6910=CARTESIAN_POINT('Ctrl Pts',(21.0520166420959,37.7957977176563,32.8188698768599));
#6911=CARTESIAN_POINT('Ctrl Pts',(20.7165511433331,37.2941045349873,33.3999131649034));
#6912=CARTESIAN_POINT('Ctrl Pts',(20.5864297301414,37.0692605098588,33.6252900637042));
#6913=CARTESIAN_POINT('Ctrl Pts',(20.3554622985991,36.5686663529566,34.0253373900292));
#6914=CARTESIAN_POINT('Ctrl Pts',(20.2549960232459,36.292215920861,34.199350083388));
#6915=CARTESIAN_POINT('Ctrl Pts',(20.1270663534886,35.8170802394984,34.4209307712032));
#6916=CARTESIAN_POINT('Ctrl Pts',(20.0790910607358,35.5879596782423,34.504026415759));
#6917=CARTESIAN_POINT('Ctrl Pts',(20.0154503117149,35.1132553852053,34.614255426495));
#6918=CARTESIAN_POINT('Ctrl Pts',(20.0000000000004,34.8675563853847,34.6410161513773));
#6919=CARTESIAN_POINT('Ctrl Pts',(20.0000000000004,34.6410161513776,34.6410161513773));
#6920=CARTESIAN_POINT('',(20.0000000000004,0.,34.6410161513773));
#6921=CARTESIAN_POINT('',(20.0000000000004,34.6410161513776,34.6410161513773));
#6922=CARTESIAN_POINT('',(20.0000000000004,0.,34.6410161513773));
#6923=CARTESIAN_POINT('Origin',(40.,40.,0.));
#6924=CARTESIAN_POINT('',(19.9999999999999,34.6410161513776,-34.6410161513776));
#6925=CARTESIAN_POINT('',(19.9999999999999,0.,-34.6410161513776));
#6926=CARTESIAN_POINT('',(19.9999999999999,34.6410161513776,-34.6410161513776));
#6927=CARTESIAN_POINT('',(30.,40.,-17.3205080756888));
#6928=CARTESIAN_POINT('Ctrl Pts',(19.9999999999999,34.6410161513776,-34.6410161513776));
#6929=CARTESIAN_POINT('Ctrl Pts',(19.9999999999999,34.9287398464594,-34.6410161513776));
#6930=CARTESIAN_POINT('Ctrl Pts',(20.0296992577666,35.2688605719923,-34.5895755279786));
#6931=CARTESIAN_POINT('Ctrl Pts',(20.1304657002358,35.8569297033293,-34.4150429299239));
#6932=CARTESIAN_POINT('Ctrl Pts',(20.2276726156403,36.2073107797085,-34.2466756135964));
#6933=CARTESIAN_POINT('Ctrl Pts',(20.4872196510673,36.9022698032704,-33.7971269612829));
#6934=CARTESIAN_POINT('Ctrl Pts',(20.7008503712725,37.2910923293497,-33.4271076998299));
#6935=CARTESIAN_POINT('Ctrl Pts',(21.1750144218796,37.9485573400285,-32.6058314730557));
#6936=CARTESIAN_POINT('Ctrl Pts',(21.4351301137511,38.2184038124865,-32.1552978788883));
#6937=CARTESIAN_POINT('Ctrl Pts',(22.2930459787064,38.9613500039003,-30.6693440121665));
#6938=CARTESIAN_POINT('Ctrl Pts',(22.9545391795447,39.2795989494824,-29.5236041794531));
#6939=CARTESIAN_POINT('Ctrl Pts',(24.3278859649791,39.7200338827688,-27.1448977706694));
#6940=CARTESIAN_POINT('Ctrl Pts',(25.0403210919701,39.8349356144784,-25.9109239336242));
#6941=CARTESIAN_POINT('Ctrl Pts',(26.4795724684824,39.9680208314247,-23.4180674246415));
#6942=CARTESIAN_POINT('Ctrl Pts',(27.2055367776954,39.986280068449,-22.1606603566028));
#6943=CARTESIAN_POINT('Ctrl Pts',(28.6316842828226,40.0021234610802,-19.690500418635));
#6944=CARTESIAN_POINT('Ctrl Pts',(29.3318666629522,40.,-18.477748961686));
#6945=CARTESIAN_POINT('Ctrl Pts',(30.,40.,-17.3205080756888));
#6946=CARTESIAN_POINT('Ctrl Pts',(30.,40.,-17.3205080756888));
#6947=CARTESIAN_POINT('Ctrl Pts',(30.6681333370477,40.,-16.1632671896916));
#6948=CARTESIAN_POINT('Ctrl Pts',(31.3683157171773,40.0021234610802,-14.9505157327426));
#6949=CARTESIAN_POINT('Ctrl Pts',(32.7944632223045,39.986280068449,-12.4803557947748));
#6950=CARTESIAN_POINT('Ctrl Pts',(33.5204275315175,39.9680208314247,-11.2229487267361));
#6951=CARTESIAN_POINT('Ctrl Pts',(34.9596789080298,39.8349356144784,-8.73009221775341));
#6952=CARTESIAN_POINT('Ctrl Pts',(35.6721140350208,39.7200338827688,-7.4961183807082));
#6953=CARTESIAN_POINT('Ctrl Pts',(37.0454608204552,39.2795989494824,-5.11741197192452));
#6954=CARTESIAN_POINT('Ctrl Pts',(37.7069540212935,38.9613500039003,-3.97167213921113));
#6955=CARTESIAN_POINT('Ctrl Pts',(38.5648698862487,38.2184038124865,-2.48571827248925));
#6956=CARTESIAN_POINT('Ctrl Pts',(38.8249855781203,37.9485573400285,-2.03518467832188));
#6957=CARTESIAN_POINT('Ctrl Pts',(39.2991496287274,37.2910923293497,-1.21390845154769));
#6958=CARTESIAN_POINT('Ctrl Pts',(39.5127803489326,36.9022698032704,-0.843889190094687));
#6959=CARTESIAN_POINT('Ctrl Pts',(39.7723273843596,36.2073107797085,-0.394340537781235));
#6960=CARTESIAN_POINT('Ctrl Pts',(39.8695342997641,35.8569297033293,-0.225973221453679));
#6961=CARTESIAN_POINT('Ctrl Pts',(39.9703007422333,35.2688605719923,-0.0514406233989685));
#6962=CARTESIAN_POINT('Ctrl Pts',(40.,34.9287398464594,-6.24836289329261E-15));
#6963=CARTESIAN_POINT('Ctrl Pts',(40.,34.6410161513776,-6.66133814775094E-15));
#6964=CARTESIAN_POINT('',(40.,0.,0.));
#6965=CARTESIAN_POINT('Origin',(19.9999999999999,40.,-34.6410161513776));
#6966=CARTESIAN_POINT('',(-20.0000000000002,34.6410161513776,-34.6410161513774));
#6967=CARTESIAN_POINT('',(-1.14175909504024E-13,40.,-34.6410161513776));
#6968=CARTESIAN_POINT('Ctrl Pts',(-20.0000000000001,34.6410161513776,-34.6410161513775));
#6969=CARTESIAN_POINT('Ctrl Pts',(-20.0000000000001,34.9287398464594,-34.6410161513775));
#6970=CARTESIAN_POINT('Ctrl Pts',(-19.9406014844668,35.2688605719923,-34.6410161513775));
#6971=CARTESIAN_POINT('Ctrl Pts',(-19.7390685995283,35.8569297033293,-34.6410161513775));
#6972=CARTESIAN_POINT('Ctrl Pts',(-19.5446547687194,36.2073107797085,-34.6410161513775));
#6973=CARTESIAN_POINT('Ctrl Pts',(-19.0255606978654,36.9022698032704,-34.6410161513775));
#6974=CARTESIAN_POINT('Ctrl Pts',(-18.5982992574549,37.2910923293497,-34.6410161513775));
#6975=CARTESIAN_POINT('Ctrl Pts',(-17.6499711562407,37.9485573400285,-34.6410161513775));
#6976=CARTESIAN_POINT('Ctrl Pts',(-17.1297397724977,38.2184038124865,-34.6410161513775));
#6977=CARTESIAN_POINT('Ctrl Pts',(-15.4139080425872,38.9613500039003,-34.6410161513775));
#6978=CARTESIAN_POINT('Ctrl Pts',(-14.0909216409105,39.2795989494824,-34.6410161513775));
#6979=CARTESIAN_POINT('Ctrl Pts',(-11.3442280700418,39.7200338827688,-34.6410161513775));
#6980=CARTESIAN_POINT('Ctrl Pts',(-9.91935781605978,39.8349356144784,-34.6410161513775));
#6981=CARTESIAN_POINT('Ctrl Pts',(-7.0408550630352,39.9680208314247,-34.6410161513775));
#6982=CARTESIAN_POINT('Ctrl Pts',(-5.5889264446091,39.986280068449,-34.6410161513775));
#6983=CARTESIAN_POINT('Ctrl Pts',(-2.73663143435478,40.0021234610802,-34.6410161513775));
#6984=CARTESIAN_POINT('Ctrl Pts',(-1.33626667409561,40.,-34.6410161513775));
#6985=CARTESIAN_POINT('Ctrl Pts',(-1.14175909504024E-13,40.,-34.6410161513775));
#6986=CARTESIAN_POINT('Ctrl Pts',(-1.13797860024079E-13,40.,-34.6410161513775));
#6987=CARTESIAN_POINT('Ctrl Pts',(1.33626667409539,40.,-34.6410161513775));
#6988=CARTESIAN_POINT('Ctrl Pts',(2.73663143435455,40.0021234610802,-34.6410161513775));
#6989=CARTESIAN_POINT('Ctrl Pts',(5.58892644460887,39.986280068449,-34.6410161513775));
#6990=CARTESIAN_POINT('Ctrl Pts',(7.04085506303497,39.9680208314247,-34.6410161513775));
#6991=CARTESIAN_POINT('Ctrl Pts',(9.91935781605956,39.8349356144784,-34.6410161513776));
#6992=CARTESIAN_POINT('Ctrl Pts',(11.3442280700416,39.7200338827688,-34.6410161513776));
#6993=CARTESIAN_POINT('Ctrl Pts',(14.0909216409102,39.2795989494824,-34.6410161513776));
#6994=CARTESIAN_POINT('Ctrl Pts',(15.413908042587,38.9613500039003,-34.6410161513776));
#6995=CARTESIAN_POINT('Ctrl Pts',(17.1297397724974,38.2184038124865,-34.6410161513776));
#6996=CARTESIAN_POINT('Ctrl Pts',(17.6499711562404,37.9485573400285,-34.6410161513776));
#6997=CARTESIAN_POINT('Ctrl Pts',(18.5982992574547,37.2910923293498,-34.6410161513776));
#6998=CARTESIAN_POINT('Ctrl Pts',(19.0255606978652,36.9022698032704,-34.6410161513776));
#6999=CARTESIAN_POINT('Ctrl Pts',(19.5446547687192,36.2073107797085,-34.6410161513776));
#7000=CARTESIAN_POINT('Ctrl Pts',(19.7390685995281,35.8569297033293,-34.6410161513776));
#7001=CARTESIAN_POINT('Ctrl Pts',(19.9406014844666,35.2688605719923,-34.6410161513776));
#7002=CARTESIAN_POINT('Ctrl Pts',(19.9999999999999,34.9287398464594,-34.6410161513776));
#7003=CARTESIAN_POINT('Ctrl Pts',(19.9999999999999,34.6410161513776,-34.6410161513776));
#7004=CARTESIAN_POINT('',(-20.0000000000001,0.,-34.6410161513775));
#7005=CARTESIAN_POINT('',(19.9999999999999,0.,-34.6410161513776));
#7006=CARTESIAN_POINT('',(-20.0000000000001,34.6410161513776,-34.6410161513775));
#7007=CARTESIAN_POINT('Origin',(-20.0000000000001,40.,-34.6410161513775));
#7008=CARTESIAN_POINT('',(-40.,34.6410161513776,2.84494650060196E-13));
#7009=CARTESIAN_POINT('',(-40.,0.,2.79318507107451E-13));
#7010=CARTESIAN_POINT('',(-40.,34.6410161513776,2.79318507107451E-13));
#7011=CARTESIAN_POINT('',(-30.0000000000001,40.,-17.3205080756886));
#7012=CARTESIAN_POINT('Ctrl Pts',(-40.,34.6410161513776,3.10862446895044E-13));
#7013=CARTESIAN_POINT('Ctrl Pts',(-40.,34.9287398464594,3.11261743733806E-13));
#7014=CARTESIAN_POINT('Ctrl Pts',(-39.9703007422333,35.2688605719923,-0.0514406233986507));
#7015=CARTESIAN_POINT('Ctrl Pts',(-39.8695342997641,35.8569297033293,-0.225973221453362));
#7016=CARTESIAN_POINT('Ctrl Pts',(-39.7723273843596,36.2073107797085,-0.394340537780919));
#7017=CARTESIAN_POINT('Ctrl Pts',(-39.5127803489326,36.9022698032704,-0.843889190094373));
#7018=CARTESIAN_POINT('Ctrl Pts',(-39.2991496287274,37.2910923293497,-1.21390845154738));
#7019=CARTESIAN_POINT('Ctrl Pts',(-38.8249855781203,37.9485573400285,-2.03518467832158));
#7020=CARTESIAN_POINT('Ctrl Pts',(-38.5648698862488,38.2184038124865,-2.48571827248894));
#7021=CARTESIAN_POINT('Ctrl Pts',(-37.7069540212935,38.9613500039003,-3.97167213921083));
#7022=CARTESIAN_POINT('Ctrl Pts',(-37.0454608204552,39.2795989494824,-5.11741197192423));
#7023=CARTESIAN_POINT('Ctrl Pts',(-35.6721140350209,39.7200338827688,-7.49611838070793));
#7024=CARTESIAN_POINT('Ctrl Pts',(-34.9596789080299,39.8349356144784,-8.73009221775313));
#7025=CARTESIAN_POINT('Ctrl Pts',(-33.5204275315176,39.9680208314247,-11.2229487267359));
#7026=CARTESIAN_POINT('Ctrl Pts',(-32.7944632223045,39.986280068449,-12.4803557947745));
#7027=CARTESIAN_POINT('Ctrl Pts',(-31.3683157171774,40.0021234610802,-14.9505157327424));
#7028=CARTESIAN_POINT('Ctrl Pts',(-30.6681333370478,40.,-16.1632671896913));
#7029=CARTESIAN_POINT('Ctrl Pts',(-30.0000000000001,40.,-17.3205080756886));
#7030=CARTESIAN_POINT('Ctrl Pts',(-30.0000000000001,40.,-17.3205080756886));
#7031=CARTESIAN_POINT('Ctrl Pts',(-29.3318666629523,40.,-18.4777489616858));
#7032=CARTESIAN_POINT('Ctrl Pts',(-28.6316842828228,40.0021234610802,-19.6905004186348));
#7033=CARTESIAN_POINT('Ctrl Pts',(-27.2055367776956,39.986280068449,-22.1606603566026));
#7034=CARTESIAN_POINT('Ctrl Pts',(-26.4795724684826,39.9680208314247,-23.4180674246413));
#7035=CARTESIAN_POINT('Ctrl Pts',(-25.0403210919703,39.8349356144784,-25.910923933624));
#7036=CARTESIAN_POINT('Ctrl Pts',(-24.3278859649793,39.7200338827688,-27.1448977706692));
#7037=CARTESIAN_POINT('Ctrl Pts',(-22.9545391795449,39.2795989494824,-29.5236041794529));
#7038=CARTESIAN_POINT('Ctrl Pts',(-22.2930459787066,38.9613500039003,-30.6693440121663));
#7039=CARTESIAN_POINT('Ctrl Pts',(-21.4351301137514,38.2184038124865,-32.1552978788882));
#7040=CARTESIAN_POINT('Ctrl Pts',(-21.1750144218799,37.9485573400285,-32.6058314730556));
#7041=CARTESIAN_POINT('Ctrl Pts',(-20.7008503712728,37.2910923293497,-33.4271076998298));
#7042=CARTESIAN_POINT('Ctrl Pts',(-20.4872196510675,36.9022698032704,-33.7971269612828));
#7043=CARTESIAN_POINT('Ctrl Pts',(-20.2276726156405,36.2073107797085,-34.2466756135962));
#7044=CARTESIAN_POINT('Ctrl Pts',(-20.1304657002361,35.8569297033293,-34.4150429299238));
#7045=CARTESIAN_POINT('Ctrl Pts',(-20.0296992577668,35.2688605719923,-34.5895755279785));
#7046=CARTESIAN_POINT('Ctrl Pts',(-20.0000000000001,34.9287398464594,-34.6410161513775));
#7047=CARTESIAN_POINT('Ctrl Pts',(-20.0000000000001,34.6410161513776,-34.6410161513775));
#7048=CARTESIAN_POINT('',(-20.0000000000001,0.,-34.6410161513775));
#7049=CARTESIAN_POINT('Origin',(-40.,40.,2.79318507107451E-13));
#7050=CARTESIAN_POINT('',(-19.9999999999997,34.6410161513776,34.6410161513777));
#7051=CARTESIAN_POINT('',(-19.9999999999997,0.,34.6410161513777));
#7052=CARTESIAN_POINT('',(-19.9999999999997,34.6410161513776,34.6410161513777));
#7053=CARTESIAN_POINT('',(-29.9999999999999,40.,17.320508075689));
#7054=CARTESIAN_POINT('Ctrl Pts',(-19.9999999999997,34.6410161513776,34.6410161513777));
#7055=CARTESIAN_POINT('Ctrl Pts',(-19.9999999999997,34.9287398464594,34.6410161513777));
#7056=CARTESIAN_POINT('Ctrl Pts',(-20.0296992577664,35.2688605719923,34.5895755279788));
#7057=CARTESIAN_POINT('Ctrl Pts',(-20.1304657002356,35.8569297033293,34.4150429299241));
#7058=CARTESIAN_POINT('Ctrl Pts',(-20.2276726156401,36.2073107797085,34.2466756135965));
#7059=CARTESIAN_POINT('Ctrl Pts',(-20.4872196510671,36.9022698032704,33.797126961283));
#7060=CARTESIAN_POINT('Ctrl Pts',(-20.7008503712723,37.2910923293498,33.4271076998301));
#7061=CARTESIAN_POINT('Ctrl Pts',(-21.1750144218794,37.9485573400285,32.6058314730559));
#7062=CARTESIAN_POINT('Ctrl Pts',(-21.4351301137509,38.2184038124865,32.1552978788885));
#7063=CARTESIAN_POINT('Ctrl Pts',(-22.2930459787062,38.9613500039003,30.6693440121666));
#7064=CARTESIAN_POINT('Ctrl Pts',(-22.9545391795445,39.2795989494824,29.5236041794532));
#7065=CARTESIAN_POINT('Ctrl Pts',(-24.3278859649789,39.7200338827688,27.1448977706696));
#7066=CARTESIAN_POINT('Ctrl Pts',(-25.0403210919699,39.8349356144784,25.9109239336244));
#7067=CARTESIAN_POINT('Ctrl Pts',(-26.4795724684822,39.9680208314247,23.4180674246416));
#7068=CARTESIAN_POINT('Ctrl Pts',(-27.2055367776953,39.986280068449,22.160660356603));
#7069=CARTESIAN_POINT('Ctrl Pts',(-28.6316842828225,40.0021234610802,19.6905004186352));
#7070=CARTESIAN_POINT('Ctrl Pts',(-29.3318666629521,40.,18.4777489616862));
#7071=CARTESIAN_POINT('Ctrl Pts',(-29.9999999999998,40.,17.320508075689));
#7072=CARTESIAN_POINT('Ctrl Pts',(-29.9999999999998,40.,17.320508075689));
#7073=CARTESIAN_POINT('Ctrl Pts',(-30.6681333370476,40.,16.1632671896918));
#7074=CARTESIAN_POINT('Ctrl Pts',(-31.3683157171772,40.0021234610802,14.9505157327428));
#7075=CARTESIAN_POINT('Ctrl Pts',(-32.7944632223044,39.986280068449,12.480355794775));
#7076=CARTESIAN_POINT('Ctrl Pts',(-33.5204275315174,39.9680208314247,11.2229487267364));
#7077=CARTESIAN_POINT('Ctrl Pts',(-34.9596789080297,39.8349356144784,8.73009221775364));
#7078=CARTESIAN_POINT('Ctrl Pts',(-35.6721140350208,39.7200338827688,7.49611838070845));
#7079=CARTESIAN_POINT('Ctrl Pts',(-37.0454608204551,39.2795989494824,5.11741197192477));
#7080=CARTESIAN_POINT('Ctrl Pts',(-37.7069540212935,38.9613500039003,3.97167213921139));
#7081=CARTESIAN_POINT('Ctrl Pts',(-38.5648698862487,38.2184038124865,2.48571827248952));
#7082=CARTESIAN_POINT('Ctrl Pts',(-38.8249855781202,37.9485573400285,2.03518467832214));
#7083=CARTESIAN_POINT('Ctrl Pts',(-39.2991496287274,37.2910923293498,1.21390845154796));
#7084=CARTESIAN_POINT('Ctrl Pts',(-39.5127803489326,36.9022698032704,0.843889190094969));
#7085=CARTESIAN_POINT('Ctrl Pts',(-39.7723273843596,36.2073107797085,0.394340537781517));
#7086=CARTESIAN_POINT('Ctrl Pts',(-39.8695342997641,35.8569297033293,0.225973221453961));
#7087=CARTESIAN_POINT('Ctrl Pts',(-39.9703007422333,35.2688605719923,0.0514406233992506));
#7088=CARTESIAN_POINT('Ctrl Pts',(-40.,34.9287398464594,2.79363226951081E-13));
#7089=CARTESIAN_POINT('Ctrl Pts',(-40.,34.6410161513776,2.79776202205539E-13));
#7090=CARTESIAN_POINT('',(-40.,0.,2.79318507107451E-13));
#7091=CARTESIAN_POINT('Origin',(-19.9999999999997,40.,34.6410161513777));
#7092=CARTESIAN_POINT('',(3.60555503696918E-13,40.,34.6410161513776));
#7093=CARTESIAN_POINT('Ctrl Pts',(20.0000000000004,34.6410161513776,34.6410161513773));
#7094=CARTESIAN_POINT('Ctrl Pts',(20.0000000000004,34.9287398464594,34.6410161513773));
#7095=CARTESIAN_POINT('Ctrl Pts',(19.940601484467,35.2688605719923,34.6410161513773));
#7096=CARTESIAN_POINT('Ctrl Pts',(19.7390685995285,35.8569297033293,34.6410161513773));
#7097=CARTESIAN_POINT('Ctrl Pts',(19.5446547687196,36.2073107797085,34.6410161513773));
#7098=CARTESIAN_POINT('Ctrl Pts',(19.0255606978656,36.9022698032704,34.6410161513773));
#7099=CARTESIAN_POINT('Ctrl Pts',(18.5982992574552,37.2910923293498,34.6410161513773));
#7100=CARTESIAN_POINT('Ctrl Pts',(17.6499711562409,37.9485573400285,34.6410161513773));
#7101=CARTESIAN_POINT('Ctrl Pts',(17.1297397724979,38.2184038124865,34.6410161513773));
#7102=CARTESIAN_POINT('Ctrl Pts',(15.4139080425874,38.9613500039003,34.6410161513774));
#7103=CARTESIAN_POINT('Ctrl Pts',(14.0909216409107,39.2795989494824,34.6410161513774));
#7104=CARTESIAN_POINT('Ctrl Pts',(11.344228070042,39.7200338827688,34.6410161513774));
#7105=CARTESIAN_POINT('Ctrl Pts',(9.91935781606003,39.8349356144784,34.6410161513774));
#7106=CARTESIAN_POINT('Ctrl Pts',(7.04085506303545,39.9680208314247,34.6410161513774));
#7107=CARTESIAN_POINT('Ctrl Pts',(5.58892644460935,39.986280068449,34.6410161513775));
#7108=CARTESIAN_POINT('Ctrl Pts',(2.73663143435502,40.0021234610802,34.6410161513775));
#7109=CARTESIAN_POINT('Ctrl Pts',(1.33626667409586,40.,34.6410161513775));
#7110=CARTESIAN_POINT('Ctrl Pts',(3.60555503696917E-13,40.,34.6410161513775));
#7111=CARTESIAN_POINT('Ctrl Pts',(3.60267371490863E-13,40.,34.6410161513775));
#7112=CARTESIAN_POINT('Ctrl Pts',(-1.33626667409514,40.,34.6410161513775));
#7113=CARTESIAN_POINT('Ctrl Pts',(-2.7366314343543,40.0021234610802,34.6410161513775));
#7114=CARTESIAN_POINT('Ctrl Pts',(-5.58892644460863,39.986280068449,34.6410161513776));
#7115=CARTESIAN_POINT('Ctrl Pts',(-7.04085506303473,39.9680208314247,34.6410161513776));
#7116=CARTESIAN_POINT('Ctrl Pts',(-9.91935781605931,39.8349356144784,34.6410161513776));
#7117=CARTESIAN_POINT('Ctrl Pts',(-11.3442280700413,39.7200338827688,34.6410161513776));
#7118=CARTESIAN_POINT('Ctrl Pts',(-14.09092164091,39.2795989494824,34.6410161513777));
#7119=CARTESIAN_POINT('Ctrl Pts',(-15.4139080425867,38.9613500039003,34.6410161513777));
#7120=CARTESIAN_POINT('Ctrl Pts',(-17.1297397724972,38.2184038124865,34.6410161513777));
#7121=CARTESIAN_POINT('Ctrl Pts',(-17.6499711562402,37.9485573400285,34.6410161513777));
#7122=CARTESIAN_POINT('Ctrl Pts',(-18.5982992574544,37.2910923293498,34.6410161513777));
#7123=CARTESIAN_POINT('Ctrl Pts',(-19.0255606978649,36.9022698032704,34.6410161513777));
#7124=CARTESIAN_POINT('Ctrl Pts',(-19.5446547687189,36.2073107797085,34.6410161513777));
#7125=CARTESIAN_POINT('Ctrl Pts',(-19.7390685995278,35.8569297033293,34.6410161513777));
#7126=CARTESIAN_POINT('Ctrl Pts',(-19.9406014844663,35.2688605719923,34.6410161513777));
#7127=CARTESIAN_POINT('Ctrl Pts',(-19.9999999999997,34.9287398464594,34.6410161513777));
#7128=CARTESIAN_POINT('Ctrl Pts',(-19.9999999999997,34.6410161513776,34.6410161513777));
#7129=CARTESIAN_POINT('',(-19.9999999999997,0.,34.6410161513777));
#7130=CARTESIAN_POINT('Origin',(0.,0.,0.));
#7131=CARTESIAN_POINT('',(-3.18408167778312E-15,0.,26.));
#7132=CARTESIAN_POINT('Origin',(0.,0.,0.));
#7133=CARTESIAN_POINT('Origin',(0.,32.,0.));
#7134=CARTESIAN_POINT('',(-3.18408167778312E-15,32.,26.));
#7135=CARTESIAN_POINT('Origin',(0.,32.,0.));
#7136=CARTESIAN_POINT('',(-3.18408167778312E-15,32.,26.));
#7137=CARTESIAN_POINT('Origin',(0.,32.,0.));
#7138=CARTESIAN_POINT('',(-1.46957615897682E-15,32.,12.));
#7139=CARTESIAN_POINT('Origin',(0.,32.,0.));
#7140=CARTESIAN_POINT('Origin',(0.,34.6410161513776,0.));
#7141=CARTESIAN_POINT('Origin',(0.,40.,0.));
#7142=CARTESIAN_POINT('Origin',(0.,34.6410161513776,0.));
#7143=CARTESIAN_POINT('Origin',(0.,40.,0.));
#7144=CARTESIAN_POINT('Origin',(0.,34.6410161513776,0.));
#7145=CARTESIAN_POINT('Origin',(0.,40.,0.));
#7146=CARTESIAN_POINT('Origin',(0.,34.6410161513776,0.));
#7147=CARTESIAN_POINT('Origin',(0.,40.,0.));
#7148=CARTESIAN_POINT('Origin',(0.,34.6410161513776,0.));
#7149=CARTESIAN_POINT('Origin',(0.,40.,0.));
#7150=CARTESIAN_POINT('Origin',(0.,34.6410161513776,0.));
#7151=CARTESIAN_POINT('Origin',(0.,40.,0.));
#7152=CARTESIAN_POINT('Origin',(0.,96.,0.));
#7153=CARTESIAN_POINT('',(-2.44929359829471E-15,96.,20.));
#7154=CARTESIAN_POINT('Origin',(0.,96.,0.));
#7155=CARTESIAN_POINT('',(-1.22464679914735E-15,96.,-10.));
#7156=CARTESIAN_POINT('Origin',(0.,96.,0.));
#7157=CARTESIAN_POINT('Origin',(0.,40.,0.));
#7158=CARTESIAN_POINT('',(-4.24230095489963E-15,40.,34.6410161513776));
#7159=CARTESIAN_POINT('Origin',(0.,62.,0.));
#7160=CARTESIAN_POINT('',(-1.46957615897682E-15,62.,12.));
#7161=CARTESIAN_POINT('Origin',(0.,62.,0.));
#7162=CARTESIAN_POINT('',(-1.46957615897682E-15,62.,12.));
#7163=CARTESIAN_POINT('Origin',(0.,62.,0.));
#7164=CARTESIAN_POINT('',(0.,62.,-10.));
#7165=CARTESIAN_POINT('Origin',(0.,62.,0.));
#7166=CARTESIAN_POINT('Origin',(0.,0.,0.));
#7167=CARTESIAN_POINT('',(-1.22464679914735E-15,0.,-10.));
#9651=UNCERTAINTY_MEASURE_WITH_UNIT(LENGTH_MEASURE(0.01),#9669,
'DISTANCE_ACCURACY_VALUE',
'Maximum model space distance between geometric entities at asserted c
onnectivities');
#9655=UNCERTAINTY_MEASURE_WITH_UNIT(LENGTH_MEASURE(0.01),#9669,
'DISTANCE_ACCURACY_VALUE',
'Maximum model space distance between geometric entities at asserted c
onnectivities');
#9664=(
GEOMETRIC_REPRESENTATION_CONTEXT(3)
GLOBAL_UNCERTAINTY_ASSIGNED_CONTEXT((#9651))
GLOBAL_UNIT_ASSIGNED_CONTEXT((#9669,#9671,#9672))
REPRESENTATION_CONTEXT('','3D')
);
#9668=(
GEOMETRIC_REPRESENTATION_CONTEXT(3)
GLOBAL_UNCERTAINTY_ASSIGNED_CONTEXT((#9655))
GLOBAL_UNIT_ASSIGNED_CONTEXT((#9669,#9671,#9672))
REPRESENTATION_CONTEXT('','3D')
);
#9669=(
LENGTH_UNIT()
NAMED_UNIT(*)
SI_UNIT(.MILLI.,.METRE.)
);
#9671=(
NAMED_UNIT(*)
PLANE_ANGLE_UNIT()
SI_UNIT($,.RADIAN.)
);
#9672=(
NAMED_UNIT(*)
SI_UNIT($,.STERADIAN.)
SOLID_ANGLE_UNIT()
);
#9681=SHAPE_DEFINITION_REPRESENTATION(#9693,#9719);
#9693=PRODUCT_DEFINITION_SHAPE('',$,#9732);
#9719=SHAPE_REPRESENTATION('',(#4292),#9664);
#9723=PRODUCT_DEFINITION_CONTEXT('part definition',#9761,'design');
#9732=PRODUCT_DEFINITION('2026-10-04-08-13-48-887','GLAND_NUT',#9744,#9723);
#9744=PRODUCT_DEFINITION_FORMATION('',$,#9771);
#9761=APPLICATION_CONTEXT(
'Core Data for Automotive Mechanical Design Process');
#9762=PRODUCT_CONTEXT('part definition',#9761,'mechanical');
#9771=PRODUCT('2026-10-04-08-13-48-887','GLAND_NUT','PART',(#9762));
#9775=PRESENTATION_STYLE_ASSIGNMENT((#9776));
#9776=SURFACE_STYLE_USAGE(.BOTH.,#9777);
#9777=SURFACE_SIDE_STYLE('',(#9778));
#9778=SURFACE_STYLE_FILL_AREA(#9779);
#9779=FILL_AREA_STYLE('Steel - Satin',(#9780));
#9780=FILL_AREA_STYLE_COLOUR('Steel - Satin',#9781);
#9781=COLOUR_RGB('Steel - Satin', 0.09019608, 0.27058824, 0.51372549);
ENDSEC;
END-ISO-10303-21;
